ISO-10303-21;
HEADER;
/* Generated by software containing ST-Developer
 * from STEP Tools, Inc. (www.steptools.com) 
 */

FILE_DESCRIPTION(
/* description */ ('PAT-054'),
/* implementation_level */ '2;1');

FILE_NAME(
/* name */ 'M5x30 frame screw.step',
/* time_stamp */ '2026-10-29T16:38:13-07:00',
/* author */ (''),
/* organization */ (''),
/* preprocessor_version */ 'ST-DEVELOPER v20.2',
/* originating_system */ 'Autodesk Translation Framework v15.17.0.0',
/* authorisation */ '');

FILE_SCHEMA (('AUTOMOTIVE_DESIGN { 1 0 10303 214 3 1 1 }'));
ENDSEC;

DATA;
#10=MECHANICAL_DESIGN_GEOMETRIC_PRESENTATION_REPRESENTATION('',(#944),#33981);
#16=ORIENTED_CLOSED_SHELL('',*,#13056,.F.);
#21=BREP_WITH_VOIDS('Body1',#13057,(#16));
#790=CONICAL_SURFACE('',#14417,0.4,0.785398163397448);
#791=CONICAL_SURFACE('',#14421,0.41,0.785398163397448);
#792=CONICAL_SURFACE('',#14425,0.26,0.463647609000806);
#841=SHAPE_REPRESENTATION_RELATIONSHIP('SRR','None',#34218,#885);
#885=ADVANCED_BREP_SHAPE_REPRESENTATION('',(#21),#33966);
#944=STYLED_ITEM('',(#34524),#21);
#1191=FACE_BOUND('',#2908,.T.);
#1192=FACE_BOUND('',#2916,.T.);
#1477=PLANE('',#14401);
#1478=PLANE('',#14402);
#1479=PLANE('',#14403);
#1480=PLANE('',#14404);
#1481=PLANE('',#14405);
#1482=PLANE('',#14406);
#1483=PLANE('',#14407);
#1484=PLANE('',#14408);
#1485=PLANE('',#14409);
#1486=PLANE('',#14414);
#1487=PLANE('',#14415);
#1488=PLANE('',#14423);
#1997=FACE_OUTER_BOUND('',#2899,.T.);
#1998=FACE_OUTER_BOUND('',#2900,.T.);
#1999=FACE_OUTER_BOUND('',#2901,.T.);
#2000=FACE_OUTER_BOUND('',#2902,.T.);
#2001=FACE_OUTER_BOUND('',#2903,.T.);
#2002=FACE_OUTER_BOUND('',#2904,.T.);
#2003=FACE_OUTER_BOUND('',#2905,.T.);
#2004=FACE_OUTER_BOUND('',#2906,.T.);
#2005=FACE_OUTER_BOUND('',#2907,.T.);
#2006=FACE_OUTER_BOUND('',#2909,.T.);
#2007=FACE_OUTER_BOUND('',#2910,.T.);
#2008=FACE_OUTER_BOUND('',#2911,.T.);
#2009=FACE_OUTER_BOUND('',#2912,.T.);
#2010=FACE_OUTER_BOUND('',#2913,.T.);
#2011=FACE_OUTER_BOUND('',#2914,.T.);
#2012=FACE_OUTER_BOUND('',#2915,.T.);
#2013=FACE_OUTER_BOUND('',#2917,.T.);
#2014=FACE_OUTER_BOUND('',#2918,.T.);
#2899=EDGE_LOOP('',(#10485,#10486,#10487,#10488));
#2900=EDGE_LOOP('',(#10489,#10490,#10491,#10492));
#2901=EDGE_LOOP('',(#10493,#10494,#10495,#10496));
#2902=EDGE_LOOP('',(#10497,#10498,#10499,#10500));
#2903=EDGE_LOOP('',(#10501,#10502,#10503,#10504));
#2904=EDGE_LOOP('',(#10505,#10506,#10507,#10508));
#2905=EDGE_LOOP('',(#10509,#10510,#10511,#10512,#10513,#10514));
#2906=EDGE_LOOP('',(#10515,#10516,#10517,#10518,#10519,#10520));
#2907=EDGE_LOOP('',(#10521));
#2908=EDGE_LOOP('',(#10522));
#2909=EDGE_LOOP('',(#10523,#10524,#10525,#10526));
#2910=EDGE_LOOP('',(#10527));
#2911=EDGE_LOOP('',(#10528));
#2912=EDGE_LOOP('',(#10529,#10530,#10531,#10532));
#2913=EDGE_LOOP('',(#10533,#10534,#10535,#10536));
#2914=EDGE_LOOP('',(#10537,#10538,#10539,#10540));
#2915=EDGE_LOOP('',(#10541));
#2916=EDGE_LOOP('',(#10542));
#2917=EDGE_LOOP('',(#10543,#10544,#10545,#10546));
#2918=EDGE_LOOP('',(#10547,#10548,#10549,#10550));
#3833=LINE('',#21272,#4767);
#3834=LINE('',#21274,#4768);
#3835=LINE('',#21276,#4769);
#3836=LINE('',#21277,#4770);
#3837=LINE('',#21280,#4771);
#3838=LINE('',#21282,#4772);
#3839=LINE('',#21283,#4773);
#3840=LINE('',#21286,#4774);
#3841=LINE('',#21288,#4775);
#3842=LINE('',#21289,#4776);
#3843=LINE('',#21292,#4777);
#3844=LINE('',#21294,#4778);
#3845=LINE('',#21295,#4779);
#3846=LINE('',#21298,#4780);
#3847=LINE('',#21300,#4781);
#3848=LINE('',#21301,#4782);
#3849=LINE('',#21303,#4783);
#3850=LINE('',#21304,#4784);
#3851=LINE('',#21314,#4785);
#3852=LINE('',#21323,#4786);
#3853=LINE('',#21327,#4787);
#3854=LINE('',#21331,#4788);
#3855=LINE('',#21338,#4789);
#3856=LINE('',#21340,#4790);
#4767=VECTOR('',#17172,1.);
#4768=VECTOR('',#17173,1.);
#4769=VECTOR('',#17174,1.);
#4770=VECTOR('',#17175,1.);
#4771=VECTOR('',#17178,1.);
#4772=VECTOR('',#17179,1.);
#4773=VECTOR('',#17180,1.);
#4774=VECTOR('',#17183,1.);
#4775=VECTOR('',#17184,1.);
#4776=VECTOR('',#17185,1.);
#4777=VECTOR('',#17188,1.);
#4778=VECTOR('',#17189,1.);
#4779=VECTOR('',#17190,1.);
#4780=VECTOR('',#17193,1.);
#4781=VECTOR('',#17194,1.);
#4782=VECTOR('',#17195,1.);
#4783=VECTOR('',#17198,1.);
#4784=VECTOR('',#17199,1.);
#4785=VECTOR('',#17212,0.25);
#4786=VECTOR('',#17225,0.4);
#4787=VECTOR('',#17230,0.425);
#4788=VECTOR('',#17235,0.41);
#4789=VECTOR('',#17244,0.26);
#4790=VECTOR('',#17247,0.25);
#5473=CIRCLE('',#14410,0.25);
#5474=CIRCLE('',#14411,0.24505);
#5475=CIRCLE('',#14413,0.25);
#5476=CIRCLE('',#14416,0.375);
#5477=CIRCLE('',#14418,0.425);
#5478=CIRCLE('',#14420,0.425);
#5479=CIRCLE('',#14422,0.395);
#5480=CIRCLE('',#14424,0.27);
#5481=CIRCLE('',#14426,0.24505);
#6251=VERTEX_POINT('',#21270);
#6252=VERTEX_POINT('',#21271);
#6253=VERTEX_POINT('',#21273);
#6254=VERTEX_POINT('',#21275);
#6255=VERTEX_POINT('',#21279);
#6256=VERTEX_POINT('',#21281);
#6257=VERTEX_POINT('',#21285);
#6258=VERTEX_POINT('',#21287);
#6259=VERTEX_POINT('',#21291);
#6260=VERTEX_POINT('',#21293);
#6261=VERTEX_POINT('',#21297);
#6262=VERTEX_POINT('',#21299);
#6263=VERTEX_POINT('',#21308);
#6264=VERTEX_POINT('',#21310);
#6265=VERTEX_POINT('',#21313);
#6266=VERTEX_POINT('',#21318);
#6267=VERTEX_POINT('',#21321);
#6268=VERTEX_POINT('',#21325);
#6269=VERTEX_POINT('',#21329);
#6270=VERTEX_POINT('',#21333);
#6271=VERTEX_POINT('',#21336);
#7742=EDGE_CURVE('',#6251,#6252,#3833,.T.);
#7743=EDGE_CURVE('',#6252,#6253,#3834,.T.);
#7744=EDGE_CURVE('',#6253,#6254,#3835,.T.);
#7745=EDGE_CURVE('',#6251,#6254,#3836,.T.);
#7746=EDGE_CURVE('',#6252,#6255,#3837,.T.);
#7747=EDGE_CURVE('',#6255,#6256,#3838,.T.);
#7748=EDGE_CURVE('',#6256,#6253,#3839,.T.);
#7749=EDGE_CURVE('',#6255,#6257,#3840,.T.);
#7750=EDGE_CURVE('',#6257,#6258,#3841,.T.);
#7751=EDGE_CURVE('',#6258,#6256,#3842,.T.);
#7752=EDGE_CURVE('',#6257,#6259,#3843,.T.);
#7753=EDGE_CURVE('',#6259,#6260,#3844,.T.);
#7754=EDGE_CURVE('',#6260,#6258,#3845,.T.);
#7755=EDGE_CURVE('',#6259,#6261,#3846,.T.);
#7756=EDGE_CURVE('',#6261,#6262,#3847,.T.);
#7757=EDGE_CURVE('',#6262,#6260,#3848,.T.);
#7758=EDGE_CURVE('',#6261,#6251,#3849,.T.);
#7759=EDGE_CURVE('',#6254,#6262,#3850,.T.);
#7760=EDGE_CURVE('',#6263,#6263,#5473,.T.);
#7761=EDGE_CURVE('',#6264,#6264,#5474,.T.);
#7762=EDGE_CURVE('',#6263,#6265,#3851,.T.);
#7763=EDGE_CURVE('',#6265,#6265,#5475,.T.);
#7764=EDGE_CURVE('',#6266,#6266,#5476,.T.);
#7765=EDGE_CURVE('',#6267,#6267,#5477,.T.);
#7766=EDGE_CURVE('',#6267,#6266,#3852,.T.);
#7767=EDGE_CURVE('',#6268,#6268,#5478,.T.);
#7768=EDGE_CURVE('',#6268,#6267,#3853,.T.);
#7769=EDGE_CURVE('',#6269,#6269,#5479,.T.);
#7770=EDGE_CURVE('',#6269,#6268,#3854,.T.);
#7771=EDGE_CURVE('',#6270,#6270,#5480,.T.);
#7772=EDGE_CURVE('',#6271,#6271,#5481,.F.);
#7773=EDGE_CURVE('',#6271,#6270,#3855,.T.);
#7774=EDGE_CURVE('',#6264,#6271,#3856,.T.);
#10485=ORIENTED_EDGE('',*,*,#7742,.T.);
#10486=ORIENTED_EDGE('',*,*,#7743,.T.);
#10487=ORIENTED_EDGE('',*,*,#7744,.T.);
#10488=ORIENTED_EDGE('',*,*,#7745,.F.);
#10489=ORIENTED_EDGE('',*,*,#7746,.T.);
#10490=ORIENTED_EDGE('',*,*,#7747,.T.);
#10491=ORIENTED_EDGE('',*,*,#7748,.T.);
#10492=ORIENTED_EDGE('',*,*,#7743,.F.);
#10493=ORIENTED_EDGE('',*,*,#7749,.T.);
#10494=ORIENTED_EDGE('',*,*,#7750,.T.);
#10495=ORIENTED_EDGE('',*,*,#7751,.T.);
#10496=ORIENTED_EDGE('',*,*,#7747,.F.);
#10497=ORIENTED_EDGE('',*,*,#7752,.T.);
#10498=ORIENTED_EDGE('',*,*,#7753,.T.);
#10499=ORIENTED_EDGE('',*,*,#7754,.T.);
#10500=ORIENTED_EDGE('',*,*,#7750,.F.);
#10501=ORIENTED_EDGE('',*,*,#7755,.T.);
#10502=ORIENTED_EDGE('',*,*,#7756,.T.);
#10503=ORIENTED_EDGE('',*,*,#7757,.T.);
#10504=ORIENTED_EDGE('',*,*,#7753,.F.);
#10505=ORIENTED_EDGE('',*,*,#7758,.T.);
#10506=ORIENTED_EDGE('',*,*,#7745,.T.);
#10507=ORIENTED_EDGE('',*,*,#7759,.T.);
#10508=ORIENTED_EDGE('',*,*,#7756,.F.);
#10509=ORIENTED_EDGE('',*,*,#7758,.F.);
#10510=ORIENTED_EDGE('',*,*,#7755,.F.);
#10511=ORIENTED_EDGE('',*,*,#7752,.F.);
#10512=ORIENTED_EDGE('',*,*,#7749,.F.);
#10513=ORIENTED_EDGE('',*,*,#7746,.F.);
#10514=ORIENTED_EDGE('',*,*,#7742,.F.);
#10515=ORIENTED_EDGE('',*,*,#7759,.F.);
#10516=ORIENTED_EDGE('',*,*,#7744,.F.);
#10517=ORIENTED_EDGE('',*,*,#7748,.F.);
#10518=ORIENTED_EDGE('',*,*,#7751,.F.);
#10519=ORIENTED_EDGE('',*,*,#7754,.F.);
#10520=ORIENTED_EDGE('',*,*,#7757,.F.);
#10521=ORIENTED_EDGE('',*,*,#7760,.T.);
#10522=ORIENTED_EDGE('',*,*,#7761,.F.);
#10523=ORIENTED_EDGE('',*,*,#7760,.F.);
#10524=ORIENTED_EDGE('',*,*,#7762,.T.);
#10525=ORIENTED_EDGE('',*,*,#7763,.T.);
#10526=ORIENTED_EDGE('',*,*,#7762,.F.);
#10527=ORIENTED_EDGE('',*,*,#7763,.F.);
#10528=ORIENTED_EDGE('',*,*,#7764,.F.);
#10529=ORIENTED_EDGE('',*,*,#7765,.F.);
#10530=ORIENTED_EDGE('',*,*,#7766,.T.);
#10531=ORIENTED_EDGE('',*,*,#7764,.T.);
#10532=ORIENTED_EDGE('',*,*,#7766,.F.);
#10533=ORIENTED_EDGE('',*,*,#7767,.F.);
#10534=ORIENTED_EDGE('',*,*,#7768,.T.);
#10535=ORIENTED_EDGE('',*,*,#7765,.T.);
#10536=ORIENTED_EDGE('',*,*,#7768,.F.);
#10537=ORIENTED_EDGE('',*,*,#7769,.F.);
#10538=ORIENTED_EDGE('',*,*,#7770,.T.);
#10539=ORIENTED_EDGE('',*,*,#7767,.T.);
#10540=ORIENTED_EDGE('',*,*,#7770,.F.);
#10541=ORIENTED_EDGE('',*,*,#7769,.T.);
#10542=ORIENTED_EDGE('',*,*,#7771,.F.);
#10543=ORIENTED_EDGE('',*,*,#7772,.F.);
#10544=ORIENTED_EDGE('',*,*,#7773,.T.);
#10545=ORIENTED_EDGE('',*,*,#7771,.T.);
#10546=ORIENTED_EDGE('',*,*,#7773,.F.);
#10547=ORIENTED_EDGE('',*,*,#7761,.T.);
#10548=ORIENTED_EDGE('',*,*,#7774,.T.);
#10549=ORIENTED_EDGE('',*,*,#7772,.T.);
#10550=ORIENTED_EDGE('',*,*,#7774,.F.);
#12105=CYLINDRICAL_SURFACE('',#14412,0.25);
#12106=CYLINDRICAL_SURFACE('',#14419,0.425);
#12107=CYLINDRICAL_SURFACE('',#14427,0.24505);
#12709=ADVANCED_FACE('',(#1997),#1477,.F.);
#12710=ADVANCED_FACE('',(#1998),#1478,.F.);
#12711=ADVANCED_FACE('',(#1999),#1479,.F.);
#12712=ADVANCED_FACE('',(#2000),#1480,.F.);
#12713=ADVANCED_FACE('',(#2001),#1481,.F.);
#12714=ADVANCED_FACE('',(#2002),#1482,.F.);
#12715=ADVANCED_FACE('',(#2003),#1483,.F.);
#12716=ADVANCED_FACE('',(#2004),#1484,.F.);
#12717=ADVANCED_FACE('',(#2005,#1191),#1485,.T.);
#12718=ADVANCED_FACE('',(#2006),#12105,.T.);
#12719=ADVANCED_FACE('',(#2007),#1486,.F.);
#12720=ADVANCED_FACE('',(#2008),#1487,.T.);
#12721=ADVANCED_FACE('',(#2009),#790,.T.);
#12722=ADVANCED_FACE('',(#2010),#12106,.T.);
#12723=ADVANCED_FACE('',(#2011),#791,.T.);
#12724=ADVANCED_FACE('',(#2012,#1192),#1488,.T.);
#12725=ADVANCED_FACE('',(#2013),#792,.T.);
#12726=ADVANCED_FACE('',(#2014),#12107,.T.);
#13056=CLOSED_SHELL('',(#12709,#12710,#12711,#12712,#12713,#12714,#12715,
#12716));
#13057=CLOSED_SHELL('',(#12717,#12718,#12719,#12720,#12721,#12722,#12723,
#12724,#12725,#12726));
#14400=AXIS2_PLACEMENT_3D('',#21268,#17168,#17169);
#14401=AXIS2_PLACEMENT_3D('',#21269,#17170,#17171);
#14402=AXIS2_PLACEMENT_3D('',#21278,#17176,#17177);
#14403=AXIS2_PLACEMENT_3D('',#21284,#17181,#17182);
#14404=AXIS2_PLACEMENT_3D('',#21290,#17186,#17187);
#14405=AXIS2_PLACEMENT_3D('',#21296,#17191,#17192);
#14406=AXIS2_PLACEMENT_3D('',#21302,#17196,#17197);
#14407=AXIS2_PLACEMENT_3D('',#21305,#17200,#17201);
#14408=AXIS2_PLACEMENT_3D('',#21306,#17202,#17203);
#14409=AXIS2_PLACEMENT_3D('',#21307,#17204,#17205);
#14410=AXIS2_PLACEMENT_3D('',#21309,#17206,#17207);
#14411=AXIS2_PLACEMENT_3D('',#21311,#17208,#17209);
#14412=AXIS2_PLACEMENT_3D('',#21312,#17210,#17211);
#14413=AXIS2_PLACEMENT_3D('',#21315,#17213,#17214);
#14414=AXIS2_PLACEMENT_3D('',#21316,#17215,#17216);
#14415=AXIS2_PLACEMENT_3D('',#21317,#17217,#17218);
#14416=AXIS2_PLACEMENT_3D('',#21319,#17219,#17220);
#14417=AXIS2_PLACEMENT_3D('',#21320,#17221,#17222);
#14418=AXIS2_PLACEMENT_3D('',#21322,#17223,#17224);
#14419=AXIS2_PLACEMENT_3D('',#21324,#17226,#17227);
#14420=AXIS2_PLACEMENT_3D('',#21326,#17228,#17229);
#14421=AXIS2_PLACEMENT_3D('',#21328,#17231,#17232);
#14422=AXIS2_PLACEMENT_3D('',#21330,#17233,#17234);
#14423=AXIS2_PLACEMENT_3D('',#21332,#17236,#17237);
#14424=AXIS2_PLACEMENT_3D('',#21334,#17238,#17239);
#14425=AXIS2_PLACEMENT_3D('',#21335,#17240,#17241);
#14426=AXIS2_PLACEMENT_3D('',#21337,#17242,#17243);
#14427=AXIS2_PLACEMENT_3D('',#21339,#17245,#17246);
#17168=DIRECTION('axis',(0.,0.,1.));
#17169=DIRECTION('refdir',(1.,0.,0.));
#17170=DIRECTION('center_axis',(0.866025403784439,0.,-0.5));
#17171=DIRECTION('ref_axis',(0.5,0.,0.866025403784439));
#17172=DIRECTION('',(-0.5,0.,-0.866025403784439));
#17173=DIRECTION('',(0.,-1.,0.));
#17174=DIRECTION('',(0.5,0.,0.866025403784439));
#17175=DIRECTION('',(0.,-1.,0.));
#17176=DIRECTION('center_axis',(1.20185167898973E-16,0.,-1.));
#17177=DIRECTION('ref_axis',(1.,0.,1.20185167898973E-16));
#17178=DIRECTION('',(-1.,0.,-1.20185167898973E-16));
#17179=DIRECTION('',(0.,-1.,0.));
#17180=DIRECTION('',(1.,0.,1.20185167898973E-16));
#17181=DIRECTION('center_axis',(-0.866025403784439,0.,-0.5));
#17182=DIRECTION('ref_axis',(0.5,0.,-0.866025403784439));
#17183=DIRECTION('',(-0.5,0.,0.866025403784439));
#17184=DIRECTION('',(0.,-1.,0.));
#17185=DIRECTION('',(0.5,0.,-0.866025403784439));
#17186=DIRECTION('center_axis',(-0.866025403784439,0.,0.5));
#17187=DIRECTION('ref_axis',(-0.5,0.,-0.866025403784439));
#17188=DIRECTION('',(0.5,0.,0.866025403784439));
#17189=DIRECTION('',(0.,-1.,0.));
#17190=DIRECTION('',(-0.5,0.,-0.866025403784439));
#17191=DIRECTION('center_axis',(-2.40370335797945E-16,0.,1.));
#17192=DIRECTION('ref_axis',(-1.,0.,-2.40370335797945E-16));
#17193=DIRECTION('',(1.,0.,2.40370335797945E-16));
#17194=DIRECTION('',(0.,-1.,0.));
#17195=DIRECTION('',(-1.,0.,-2.40370335797945E-16));
#17196=DIRECTION('center_axis',(0.866025403784439,0.,0.5));
#17197=DIRECTION('ref_axis',(-0.5,0.,0.866025403784439));
#17198=DIRECTION('',(0.5,0.,-0.866025403784439));
#17199=DIRECTION('',(-0.5,0.,0.866025403784439));
#17200=DIRECTION('center_axis',(0.,1.,0.));
#17201=DIRECTION('ref_axis',(1.,0.,0.));
#17202=DIRECTION('center_axis',(0.,-1.,0.));
#17203=DIRECTION('ref_axis',(0.,0.,-1.));
#17204=DIRECTION('center_axis',(0.,1.,0.));
#17205=DIRECTION('ref_axis',(1.,0.,0.));
#17206=DIRECTION('center_axis',(0.,1.,0.));
#17207=DIRECTION('ref_axis',(1.,0.,0.));
#17208=DIRECTION('center_axis',(0.,1.,0.));
#17209=DIRECTION('ref_axis',(1.,0.,0.));
#17210=DIRECTION('center_axis',(0.,1.,0.));
#17211=DIRECTION('ref_axis',(1.,0.,0.));
#17212=DIRECTION('',(0.,-1.,0.));
#17213=DIRECTION('center_axis',(0.,1.,0.));
#17214=DIRECTION('ref_axis',(1.,0.,0.));
#17215=DIRECTION('center_axis',(0.,1.,0.));
#17216=DIRECTION('ref_axis',(1.,0.,0.));
#17217=DIRECTION('center_axis',(0.,1.,0.));
#17218=DIRECTION('ref_axis',(0.,0.,1.));
#17219=DIRECTION('center_axis',(0.,-1.,0.));
#17220=DIRECTION('ref_axis',(1.,0.,0.));
#17221=DIRECTION('center_axis',(0.,-1.,0.));
#17222=DIRECTION('ref_axis',(1.,0.,0.));
#17223=DIRECTION('center_axis',(0.,-1.,0.));
#17224=DIRECTION('ref_axis',(1.,0.,0.));
#17225=DIRECTION('',(0.707106781186548,0.707106781186547,8.65956056235493E-17));
#17226=DIRECTION('center_axis',(0.,-1.,0.));
#17227=DIRECTION('ref_axis',(1.,0.,0.));
#17228=DIRECTION('center_axis',(0.,-1.,0.));
#17229=DIRECTION('ref_axis',(1.,0.,0.));
#17230=DIRECTION('',(0.,1.,0.));
#17231=DIRECTION('center_axis',(0.,1.,0.));
#17232=DIRECTION('ref_axis',(1.,0.,0.));
#17233=DIRECTION('center_axis',(0.,-1.,0.));
#17234=DIRECTION('ref_axis',(1.,0.,0.));
#17235=DIRECTION('',(-0.707106781186547,0.707106781186548,-8.65956056235493E-17));
#17236=DIRECTION('center_axis',(0.,-1.,0.));
#17237=DIRECTION('ref_axis',(0.,0.,-1.));
#17238=DIRECTION('center_axis',(0.,-1.,0.));
#17239=DIRECTION('ref_axis',(1.,0.,0.));
#17240=DIRECTION('center_axis',(0.,1.,0.));
#17241=DIRECTION('ref_axis',(1.,0.,0.));
#17242=DIRECTION('center_axis',(0.,1.,0.));
#17243=DIRECTION('ref_axis',(1.,0.,0.));
#17244=DIRECTION('',(-0.447213595499958,0.894427190999916,-5.47678698264203E-17));
#17245=DIRECTION('center_axis',(0.,-1.,0.));
#17246=DIRECTION('ref_axis',(1.,0.,0.));
#17247=DIRECTION('',(0.,1.,0.));
#21268=CARTESIAN_POINT('',(0.,0.,0.));
#21269=CARTESIAN_POINT('Origin',(0.115470053837925,-0.5,-0.2));
#21270=CARTESIAN_POINT('',(0.23094010767585,-0.5,0.));
#21271=CARTESIAN_POINT('',(0.115470053837925,-0.5,-0.2));
#21272=CARTESIAN_POINT('',(0.23094010767585,-0.5,0.));
#21273=CARTESIAN_POINT('',(0.115470053837925,-0.8,-0.2));
#21274=CARTESIAN_POINT('',(0.115470053837925,-0.5,-0.2));
#21275=CARTESIAN_POINT('',(0.23094010767585,-0.8,0.));
#21276=CARTESIAN_POINT('',(0.23094010767585,-0.8,0.));
#21277=CARTESIAN_POINT('',(0.23094010767585,-0.5,0.));
#21278=CARTESIAN_POINT('Origin',(-0.115470053837925,-0.5,-0.2));
#21279=CARTESIAN_POINT('',(-0.115470053837925,-0.5,-0.2));
#21280=CARTESIAN_POINT('',(0.115470053837925,-0.5,-0.2));
#21281=CARTESIAN_POINT('',(-0.115470053837925,-0.8,-0.2));
#21282=CARTESIAN_POINT('',(-0.115470053837925,-0.5,-0.2));
#21283=CARTESIAN_POINT('',(0.115470053837925,-0.8,-0.2));
#21284=CARTESIAN_POINT('Origin',(-0.23094010767585,-0.5,-2.77555756156289E-17));
#21285=CARTESIAN_POINT('',(-0.23094010767585,-0.5,-2.82820063659975E-17));
#21286=CARTESIAN_POINT('',(-0.115470053837925,-0.5,-0.2));
#21287=CARTESIAN_POINT('',(-0.23094010767585,-0.8,-2.77555756156289E-17));
#21288=CARTESIAN_POINT('',(-0.23094010767585,-0.5,-2.82820063659975E-17));
#21289=CARTESIAN_POINT('',(-0.115470053837925,-0.8,-0.2));
#21290=CARTESIAN_POINT('Origin',(-0.115470053837925,-0.5,0.2));
#21291=CARTESIAN_POINT('',(-0.115470053837925,-0.5,0.2));
#21292=CARTESIAN_POINT('',(-0.23094010767585,-0.5,-2.82820063659975E-17));
#21293=CARTESIAN_POINT('',(-0.115470053837925,-0.8,0.2));
#21294=CARTESIAN_POINT('',(-0.115470053837925,-0.5,0.2));
#21295=CARTESIAN_POINT('',(-0.23094010767585,-0.8,-2.82820063659975E-17));
#21296=CARTESIAN_POINT('Origin',(0.115470053837925,-0.5,0.2));
#21297=CARTESIAN_POINT('',(0.115470053837925,-0.5,0.2));
#21298=CARTESIAN_POINT('',(-0.115470053837925,-0.5,0.2));
#21299=CARTESIAN_POINT('',(0.115470053837925,-0.8,0.2));
#21300=CARTESIAN_POINT('',(0.115470053837925,-0.5,0.2));
#21301=CARTESIAN_POINT('',(-0.115470053837925,-0.8,0.2));
#21302=CARTESIAN_POINT('Origin',(0.23094010767585,-0.5,0.));
#21303=CARTESIAN_POINT('',(0.115470053837925,-0.5,0.2));
#21304=CARTESIAN_POINT('',(0.115470053837925,-0.8,0.2));
#21305=CARTESIAN_POINT('Origin',(0.,-0.5,0.));
#21306=CARTESIAN_POINT('Origin',(0.,-0.8,0.));
#21307=CARTESIAN_POINT('Origin',(0.,-1.9,0.));
#21308=CARTESIAN_POINT('',(-0.25,-1.9,3.06161699786838E-17));
#21309=CARTESIAN_POINT('Origin',(0.,-1.9,0.));
#21310=CARTESIAN_POINT('',(-0.24505,-1.9,3.00099698131059E-17));
#21311=CARTESIAN_POINT('Origin',(0.,-1.9,0.));
#21312=CARTESIAN_POINT('Origin',(0.,-3.,0.));
#21313=CARTESIAN_POINT('',(-0.25,-3.,3.06161699786838E-17));
#21314=CARTESIAN_POINT('',(-0.25,-3.,3.06161699786838E-17));
#21315=CARTESIAN_POINT('Origin',(0.,-3.,0.));
#21316=CARTESIAN_POINT('Origin',(0.,-3.,0.));
#21317=CARTESIAN_POINT('Origin',(0.375,0.5,0.));
#21318=CARTESIAN_POINT('',(-0.375,0.5,-4.59242549680257E-17));
#21319=CARTESIAN_POINT('Origin',(0.,0.5,0.));
#21320=CARTESIAN_POINT('Origin',(0.,0.475,0.));
#21321=CARTESIAN_POINT('',(-0.425,0.45,-5.20474889637625E-17));
#21322=CARTESIAN_POINT('Origin',(0.,0.45,0.));
#21323=CARTESIAN_POINT('',(-0.4,0.475,-4.89858719658941E-17));
#21324=CARTESIAN_POINT('Origin',(0.,0.24,0.));
#21325=CARTESIAN_POINT('',(-0.425,0.0299999999999998,-5.20474889637625E-17));
#21326=CARTESIAN_POINT('Origin',(0.,0.0299999999999998,0.));
#21327=CARTESIAN_POINT('',(-0.425,0.24,-5.20474889637625E-17));
#21328=CARTESIAN_POINT('Origin',(0.,0.0150000000000001,0.));
#21329=CARTESIAN_POINT('',(-0.395,4.85722573273506E-17,-4.83735485663204E-17));
#21330=CARTESIAN_POINT('Origin',(0.,0.,0.));
#21331=CARTESIAN_POINT('',(-0.41,0.0150000000000001,-5.02105187650415E-17));
#21332=CARTESIAN_POINT('Origin',(0.27,0.,0.));
#21333=CARTESIAN_POINT('',(-0.27,0.,-3.30654635769785E-17));
#21334=CARTESIAN_POINT('Origin',(0.,0.,0.));
#21335=CARTESIAN_POINT('Origin',(0.,-0.02,0.));
#21336=CARTESIAN_POINT('',(-0.24505,-0.0498999999999999,3.00099698131059E-17));
#21337=CARTESIAN_POINT('Origin',(0.,-0.0498999999999999,0.));
#21338=CARTESIAN_POINT('',(-0.26,-0.02,-3.18408167778312E-17));
#21339=CARTESIAN_POINT('Origin',(0.,-0.995,0.));
#21340=CARTESIAN_POINT('',(-0.24505,-0.995,-3.00099698131059E-17));
#33914=UNCERTAINTY_MEASURE_WITH_UNIT(LENGTH_MEASURE(0.001),#33982,
'DISTANCE_ACCURACY_VALUE',
'Maximum model space distance between geometric entities at asserted c
onnectivities');
#33929=UNCERTAINTY_MEASURE_WITH_UNIT(LENGTH_MEASURE(0.001),#33982,
'DISTANCE_ACCURACY_VALUE',
'Maximum model space distance between geometric entities at asserted c
onnectivities');
#33966=(
GEOMETRIC_REPRESENTATION_CONTEXT(3)
GLOBAL_UNCERTAINTY_ASSIGNED_CONTEXT((#33914))
GLOBAL_UNIT_ASSIGNED_CONTEXT((#33982,#33984,#33985))
REPRESENTATION_CONTEXT('','3D')
);
#33981=(
GEOMETRIC_REPRESENTATION_CONTEXT(3)
GLOBAL_UNCERTAINTY_ASSIGNED_CONTEXT((#33929))
GLOBAL_UNIT_ASSIGNED_CONTEXT((#33982,#33984,#33985))
REPRESENTATION_CONTEXT('','3D')
);
#33982=(
LENGTH_UNIT()
NAMED_UNIT(*)
SI_UNIT(.CENTI.,.METRE.)
);
#33984=(
NAMED_UNIT(*)
PLANE_ANGLE_UNIT()
SI_UNIT($,.RADIAN.)
);
#33985=(
NAMED_UNIT(*)
SI_UNIT($,.STERADIAN.)
SOLID_ANGLE_UNIT()
);
#34022=SHAPE_DEFINITION_REPRESENTATION(#34086,#34218);
#34086=PRODUCT_DEFINITION_SHAPE('',$,#34270);
#34218=SHAPE_REPRESENTATION('',(#14400),#33966);
#34233=PRODUCT_DEFINITION_CONTEXT('part definition',#34388,'design');
#34270=PRODUCT_DEFINITION('M5x30 frame screw','M5x30 frame screw',#34321,
#34233);
#34321=PRODUCT_DEFINITION_FORMATION('',$,#34426);
#34388=APPLICATION_CONTEXT(
'Core Data for Automotive Mechanical Design Process');
#34389=PRODUCT_CONTEXT('part definition',#34388,'mechanical');
#34426=PRODUCT('M5x30 frame screw','M5x30 frame screw',
'M5x30 frame screw',(#34389));
#34518=COLOUR_RGB('Black',0.12,0.14,0.17);
#34519=FILL_AREA_STYLE_COLOUR('',#34518);
#34520=FILL_AREA_STYLE('',(#34519));
#34521=SURFACE_STYLE_FILL_AREA(#34520);
#34522=SURFACE_SIDE_STYLE('',(#34521));
#34523=SURFACE_STYLE_USAGE(.BOTH.,#34522);
#34524=PRESENTATION_STYLE_ASSIGNMENT((#34523));
ENDSEC;
END-ISO-10303-21;
